ISO-10303-21;
HEADER;
/* Generated by software containing ST-Developer
 * from STEP Tools, Inc. (www.steptools.com) 
 */

FILE_DESCRIPTION(
/* description */ ('Four-bar parallelogram arm'),
/* implementation_level */ '2;1');

FILE_NAME(
/* name */ 'Outer race spacer (3).step',
/* time_stamp */ '2026-10-28T03:24:55-07:00',
/* author */ (''),
/* organization */ (''),
/* preprocessor_version */ 'ST-DEVELOPER v20.2',
/* originating_system */ 'Autodesk Translation Framework v15.17.0.0',
/* authorisation */ '');

FILE_SCHEMA (('AUTOMOTIVE_DESIGN { 1 0 10303 214 3 1 1 }'));
ENDSEC;

DATA;
#10=MECHANICAL_DESIGN_GEOMETRIC_PRESENTATION_REPRESENTATION('',(#651),#14512);
#551=SHAPE_REPRESENTATION_RELATIONSHIP('SRR','None',#14774,#601);
#601=ADVANCED_BREP_SHAPE_REPRESENTATION('',(#708),#14489);
#651=STYLED_ITEM('',(#15087),#708);
#708=MANIFOLD_SOLID_BREP('Body1',#7356);
#915=FACE_BOUND('',#2043,.T.);
#916=FACE_BOUND('',#2045,.T.);
#1121=PLANE('',#8462);
#1122=PLANE('',#8463);
#1440=FACE_OUTER_BOUND('',#2040,.T.);
#1441=FACE_OUTER_BOUND('',#2041,.T.);
#1442=FACE_OUTER_BOUND('',#2042,.T.);
#1443=FACE_OUTER_BOUND('',#2044,.T.);
#2040=EDGE_LOOP('',(#6000,#6001,#6002,#6003));
#2041=EDGE_LOOP('',(#6004,#6005,#6006,#6007));
#2042=EDGE_LOOP('',(#6008));
#2043=EDGE_LOOP('',(#6009));
#2044=EDGE_LOOP('',(#6010));
#2045=EDGE_LOOP('',(#6011));
#2566=LINE('',#13148,#2960);
#2567=LINE('',#13154,#2961);
#2960=VECTOR('',#10264,1.02);
#2961=VECTOR('',#10271,1.49);
#3346=CIRCLE('',#8457,1.02);
#3347=CIRCLE('',#8458,1.02);
#3348=CIRCLE('',#8460,1.49);
#3349=CIRCLE('',#8461,1.49);
#3880=VERTEX_POINT('',#13145);
#3881=VERTEX_POINT('',#13147);
#3882=VERTEX_POINT('',#13151);
#3883=VERTEX_POINT('',#13153);
#4631=EDGE_CURVE('',#3880,#3880,#3346,.T.);
#4632=EDGE_CURVE('',#3880,#3881,#2566,.T.);
#4633=EDGE_CURVE('',#3881,#3881,#3347,.T.);
#4634=EDGE_CURVE('',#3882,#3882,#3348,.T.);
#4635=EDGE_CURVE('',#3882,#3883,#2567,.T.);
#4636=EDGE_CURVE('',#3883,#3883,#3349,.T.);
#6000=ORIENTED_EDGE('',*,*,#4631,.F.);
#6001=ORIENTED_EDGE('',*,*,#4632,.T.);
#6002=ORIENTED_EDGE('',*,*,#4633,.T.);
#6003=ORIENTED_EDGE('',*,*,#4632,.F.);
#6004=ORIENTED_EDGE('',*,*,#4634,.F.);
#6005=ORIENTED_EDGE('',*,*,#4635,.T.);
#6006=ORIENTED_EDGE('',*,*,#4636,.T.);
#6007=ORIENTED_EDGE('',*,*,#4635,.F.);
#6008=ORIENTED_EDGE('',*,*,#4634,.T.);
#6009=ORIENTED_EDGE('',*,*,#4631,.T.);
#6010=ORIENTED_EDGE('',*,*,#4636,.F.);
#6011=ORIENTED_EDGE('',*,*,#4633,.F.);
#6834=CYLINDRICAL_SURFACE('',#8456,1.02);
#6835=CYLINDRICAL_SURFACE('',#8459,1.49);
#7145=ADVANCED_FACE('',(#1440),#6834,.F.);
#7146=ADVANCED_FACE('',(#1441),#6835,.T.);
#7147=ADVANCED_FACE('',(#1442,#915),#1121,.T.);
#7148=ADVANCED_FACE('',(#1443,#916),#1122,.F.);
#7356=CLOSED_SHELL('',(#7145,#7146,#7147,#7148));
#8455=AXIS2_PLACEMENT_3D('',#13143,#10258,#10259);
#8456=AXIS2_PLACEMENT_3D('',#13144,#10260,#10261);
#8457=AXIS2_PLACEMENT_3D('',#13146,#10262,#10263);
#8458=AXIS2_PLACEMENT_3D('',#13149,#10265,#10266);
#8459=AXIS2_PLACEMENT_3D('',#13150,#10267,#10268);
#8460=AXIS2_PLACEMENT_3D('',#13152,#10269,#10270);
#8461=AXIS2_PLACEMENT_3D('',#13155,#10272,#10273);
#8462=AXIS2_PLACEMENT_3D('',#13156,#10274,#10275);
#8463=AXIS2_PLACEMENT_3D('',#13157,#10276,#10277);
#10258=DIRECTION('axis',(0.,0.,1.));
#10259=DIRECTION('refdir',(1.,0.,0.));
#10260=DIRECTION('center_axis',(0.,1.,0.));
#10261=DIRECTION('ref_axis',(1.,0.,0.));
#10262=DIRECTION('center_axis',(0.,-1.,0.));
#10263=DIRECTION('ref_axis',(1.,0.,0.));
#10264=DIRECTION('',(0.,-1.,0.));
#10265=DIRECTION('center_axis',(0.,-1.,0.));
#10266=DIRECTION('ref_axis',(1.,0.,0.));
#10267=DIRECTION('center_axis',(0.,1.,0.));
#10268=DIRECTION('ref_axis',(1.,0.,0.));
#10269=DIRECTION('center_axis',(0.,1.,0.));
#10270=DIRECTION('ref_axis',(1.,0.,0.));
#10271=DIRECTION('',(0.,-1.,0.));
#10272=DIRECTION('center_axis',(0.,1.,0.));
#10273=DIRECTION('ref_axis',(1.,0.,0.));
#10274=DIRECTION('center_axis',(0.,1.,0.));
#10275=DIRECTION('ref_axis',(1.,0.,0.));
#10276=DIRECTION('center_axis',(0.,1.,0.));
#10277=DIRECTION('ref_axis',(1.,0.,0.));
#13143=CARTESIAN_POINT('',(0.,0.,0.));
#13144=CARTESIAN_POINT('Origin',(20.,-0.15,14.));
#13145=CARTESIAN_POINT('',(18.98,0.15,14.));
#13146=CARTESIAN_POINT('Origin',(20.,0.15,14.));
#13147=CARTESIAN_POINT('',(18.98,-0.15,14.));
#13148=CARTESIAN_POINT('',(18.98,-0.15,14.));
#13149=CARTESIAN_POINT('Origin',(20.,-0.15,14.));
#13150=CARTESIAN_POINT('Origin',(20.,-0.15,14.));
#13151=CARTESIAN_POINT('',(18.51,0.15,14.));
#13152=CARTESIAN_POINT('Origin',(20.,0.15,14.));
#13153=CARTESIAN_POINT('',(18.51,-0.15,14.));
#13154=CARTESIAN_POINT('',(18.51,-0.15,14.));
#13155=CARTESIAN_POINT('Origin',(20.,-0.15,14.));
#13156=CARTESIAN_POINT('Origin',(20.,0.15,14.));
#13157=CARTESIAN_POINT('Origin',(20.,-0.15,14.));
#14432=UNCERTAINTY_MEASURE_WITH_UNIT(LENGTH_MEASURE(0.001),#14513,
'DISTANCE_ACCURACY_VALUE',
'Maximum model space distance between geometric entities at asserted c
onnectivities');
#14455=UNCERTAINTY_MEASURE_WITH_UNIT(LENGTH_MEASURE(0.001),#14513,
'DISTANCE_ACCURACY_VALUE',
'Maximum model space distance between geometric entities at asserted c
onnectivities');
#14489=(
GEOMETRIC_REPRESENTATION_CONTEXT(3)
GLOBAL_UNCERTAINTY_ASSIGNED_CONTEXT((#14432))
GLOBAL_UNIT_ASSIGNED_CONTEXT((#14513,#14515,#14516))
REPRESENTATION_CONTEXT('','3D')
);
#14512=(
GEOMETRIC_REPRESENTATION_CONTEXT(3)
GLOBAL_UNCERTAINTY_ASSIGNED_CONTEXT((#14455))
GLOBAL_UNIT_ASSIGNED_CONTEXT((#14513,#14515,#14516))
REPRESENTATION_CONTEXT('','3D')
);
#14513=(
LENGTH_UNIT()
NAMED_UNIT(*)
SI_UNIT(.CENTI.,.METRE.)
);
#14515=(
NAMED_UNIT(*)
PLANE_ANGLE_UNIT()
SI_UNIT($,.RADIAN.)
);
#14516=(
NAMED_UNIT(*)
SI_UNIT($,.STERADIAN.)
SOLID_ANGLE_UNIT()
);
#14550=SHAPE_DEFINITION_REPRESENTATION(#14606,#14774);
#14606=PRODUCT_DEFINITION_SHAPE('',$,#14831);
#14774=SHAPE_REPRESENTATION('',(#8455),#14489);
#14797=PRODUCT_DEFINITION_CONTEXT('part definition',#14967,'design');
#14831=PRODUCT_DEFINITION('Outer race spacer (3)','Outer race spacer (3)',
#14887,#14797);
#14887=PRODUCT_DEFINITION_FORMATION('',$,#15002);
#14967=APPLICATION_CONTEXT(
'Core Data for Automotive Mechanical Design Process');
#14968=PRODUCT_CONTEXT('part definition',#14967,'mechanical');
#15002=PRODUCT('Outer race spacer (3)','Outer race spacer (3)',
'Outer race spacer (3)',(#14968));
#15081=COLOUR_RGB('Grey',0.48,0.52,0.57);
#15082=FILL_AREA_STYLE_COLOUR('',#15081);
#15083=FILL_AREA_STYLE('',(#15082));
#15084=SURFACE_STYLE_FILL_AREA(#15083);
#15085=SURFACE_SIDE_STYLE('',(#15084));
#15086=SURFACE_STYLE_USAGE(.BOTH.,#15085);
#15087=PRESENTATION_STYLE_ASSIGNMENT((#15086));
ENDSEC;
END-ISO-10303-21;
